ISO-10303-21;
HEADER;
/* Generated by software containing ST-Developer
 * from STEP Tools, Inc. (www.steptools.com) 
 */

FILE_DESCRIPTION(
/* description */ ('Belt tension measurement rig'),
/* implementation_level */ '2;1');

FILE_NAME(
/* name */ 'Input M3 set screw (1).step',
/* time_stamp */ '2026-10-28T03:24:44-07:00',
/* author */ (''),
/* organization */ (''),
/* preprocessor_version */ 'ST-DEVELOPER v20.2',
/* originating_system */ 'Autodesk Translation Framework v15.17.0.0',
/* authorisation */ '');

FILE_SCHEMA (('AUTOMOTIVE_DESIGN { 1 0 10303 214 3 1 1 }'));
ENDSEC;

DATA;
#10=MECHANICAL_DESIGN_GEOMETRIC_PRESENTATION_REPRESENTATION('',(#748),#23587);
#623=SHAPE_REPRESENTATION_RELATIONSHIP('SRR','None',#23873,#678);
#678=ADVANCED_BREP_SHAPE_REPRESENTATION('',(#816),#23571);
#748=STYLED_ITEM('',(#24218),#816);
#816=MANIFOLD_SOLID_BREP('Body1',#12255);
#1290=PLANE('',#13860);
#1291=PLANE('',#13861);
#1823=FACE_OUTER_BOUND('',#2691,.T.);
#1824=FACE_OUTER_BOUND('',#2692,.T.);
#1825=FACE_OUTER_BOUND('',#2693,.T.);
#2691=EDGE_LOOP('',(#9986,#9987,#9988,#9989));
#2692=EDGE_LOOP('',(#9990));
#2693=EDGE_LOOP('',(#9991));
#3504=LINE('',#21530,#4255);
#4255=VECTOR('',#17019,0.15);
#4918=CIRCLE('',#13858,0.15);
#4919=CIRCLE('',#13859,0.15);
#5933=VERTEX_POINT('',#21527);
#5934=VERTEX_POINT('',#21529);
#7352=EDGE_CURVE('',#5933,#5933,#4918,.T.);
#7353=EDGE_CURVE('',#5933,#5934,#3504,.T.);
#7354=EDGE_CURVE('',#5934,#5934,#4919,.T.);
#9986=ORIENTED_EDGE('',*,*,#7352,.F.);
#9987=ORIENTED_EDGE('',*,*,#7353,.T.);
#9988=ORIENTED_EDGE('',*,*,#7354,.T.);
#9989=ORIENTED_EDGE('',*,*,#7353,.F.);
#9990=ORIENTED_EDGE('',*,*,#7352,.T.);
#9991=ORIENTED_EDGE('',*,*,#7354,.F.);
#11328=CYLINDRICAL_SURFACE('',#13857,0.15);
#11964=ADVANCED_FACE('',(#1823),#11328,.T.);
#11965=ADVANCED_FACE('',(#1824),#1290,.T.);
#11966=ADVANCED_FACE('',(#1825),#1291,.F.);
#12255=CLOSED_SHELL('',(#11964,#11965,#11966));
#13856=AXIS2_PLACEMENT_3D('',#21525,#17013,#17014);
#13857=AXIS2_PLACEMENT_3D('',#21526,#17015,#17016);
#13858=AXIS2_PLACEMENT_3D('',#21528,#17017,#17018);
#13859=AXIS2_PLACEMENT_3D('',#21531,#17020,#17021);
#13860=AXIS2_PLACEMENT_3D('',#21532,#17022,#17023);
#13861=AXIS2_PLACEMENT_3D('',#21533,#17024,#17025);
#17013=DIRECTION('axis',(0.,0.,1.));
#17014=DIRECTION('refdir',(1.,0.,0.));
#17015=DIRECTION('center_axis',(0.,0.,1.));
#17016=DIRECTION('ref_axis',(1.,0.,0.));
#17017=DIRECTION('center_axis',(0.,0.,1.));
#17018=DIRECTION('ref_axis',(1.,0.,0.));
#17019=DIRECTION('',(0.,0.,-1.));
#17020=DIRECTION('center_axis',(0.,0.,1.));
#17021=DIRECTION('ref_axis',(1.,0.,0.));
#17022=DIRECTION('center_axis',(0.,0.,1.));
#17023=DIRECTION('ref_axis',(1.,0.,0.));
#17024=DIRECTION('center_axis',(0.,0.,1.));
#17025=DIRECTION('ref_axis',(1.,0.,0.));
#21525=CARTESIAN_POINT('',(0.,0.,0.));
#21526=CARTESIAN_POINT('Origin',(0.,-3.95,7.4));
#21527=CARTESIAN_POINT('',(-0.15,-3.95,7.65));
#21528=CARTESIAN_POINT('Origin',(0.,-3.95,7.65));
#21529=CARTESIAN_POINT('',(-0.15,-3.95,7.4));
#21530=CARTESIAN_POINT('',(-0.15,-3.95,7.4));
#21531=CARTESIAN_POINT('Origin',(0.,-3.95,7.4));
#21532=CARTESIAN_POINT('Origin',(0.,-3.95,7.65));
#21533=CARTESIAN_POINT('Origin',(0.,-3.95,7.4));
#23506=UNCERTAINTY_MEASURE_WITH_UNIT(LENGTH_MEASURE(0.001),#23588,
'DISTANCE_ACCURACY_VALUE',
'Maximum model space distance between geometric entities at asserted c
onnectivities');
#23522=UNCERTAINTY_MEASURE_WITH_UNIT(LENGTH_MEASURE(0.001),#23588,
'DISTANCE_ACCURACY_VALUE',
'Maximum model space distance between geometric entities at asserted c
onnectivities');
#23571=(
GEOMETRIC_REPRESENTATION_CONTEXT(3)
GLOBAL_UNCERTAINTY_ASSIGNED_CONTEXT((#23506))
GLOBAL_UNIT_ASSIGNED_CONTEXT((#23588,#23590,#23591))
REPRESENTATION_CONTEXT('','3D')
);
#23587=(
GEOMETRIC_REPRESENTATION_CONTEXT(3)
GLOBAL_UNCERTAINTY_ASSIGNED_CONTEXT((#23522))
GLOBAL_UNIT_ASSIGNED_CONTEXT((#23588,#23590,#23591))
REPRESENTATION_CONTEXT('','3D')
);
#23588=(
LENGTH_UNIT()
NAMED_UNIT(*)
SI_UNIT(.CENTI.,.METRE.)
);
#23590=(
NAMED_UNIT(*)
PLANE_ANGLE_UNIT()
SI_UNIT($,.RADIAN.)
);
#23591=(
NAMED_UNIT(*)
SI_UNIT($,.STERADIAN.)
SOLID_ANGLE_UNIT()
);
#23640=SHAPE_DEFINITION_REPRESENTATION(#23717,#23873);
#23717=PRODUCT_DEFINITION_SHAPE('',$,#23938);
#23873=SHAPE_REPRESENTATION('',(#13856),#23571);
#23889=PRODUCT_DEFINITION_CONTEXT('part definition',#24083,'design');
#23938=PRODUCT_DEFINITION('Input M3 set screw (1)',
'Input M3 set screw (1)',#24002,#23889);
#24002=PRODUCT_DEFINITION_FORMATION('',$,#24133);
#24083=APPLICATION_CONTEXT(
'Core Data for Automotive Mechanical Design Process');
#24084=PRODUCT_CONTEXT('part definition',#24083,'mechanical');
#24133=PRODUCT('Input M3 set screw (1)','Input M3 set screw (1)',
'Input M3 set screw (1)',(#24084));
#24212=COLOUR_RGB('Black',0.12,0.14,0.17);
#24213=FILL_AREA_STYLE_COLOUR('',#24212);
#24214=FILL_AREA_STYLE('',(#24213));
#24215=SURFACE_STYLE_FILL_AREA(#24214);
#24216=SURFACE_SIDE_STYLE('',(#24215));
#24217=SURFACE_STYLE_USAGE(.BOTH.,#24216);
#24218=PRESENTATION_STYLE_ASSIGNMENT((#24217));
ENDSEC;
END-ISO-10303-21;
